ISO-10303-21;
HEADER;
/* Generated by software containing ST-Developer
 * from STEP Tools, Inc. (www.steptools.com) 
 */

FILE_DESCRIPTION(
/* description */ (''),
/* implementation_level */ '2;1');

FILE_NAME(
/* name */ 'Blade_04.step',
/* time_stamp */ '2026-10-23T22:28:14+06:00',
/* author */ (''),
/* organization */ (''),
/* preprocessor_version */ 'ST-DEVELOPER v20.2',
/* originating_system */ 'Autodesk Translation Framework v15.15.0.0',
/* authorisation */ '');

FILE_SCHEMA (('AUTOMOTIVE_DESIGN { 1 0 10303 214 3 1 1 }'));
ENDSEC;

DATA;
#10=MECHANICAL_DESIGN_GEOMETRIC_PRESENTATION_REPRESENTATION('',(#115),#6753);
#89=SHAPE_REPRESENTATION_RELATIONSHIP('SRR','None',#6812,#102);
#102=ADVANCED_BREP_SHAPE_REPRESENTATION('',(#128),#6752);
#115=STYLED_ITEM('',(#6914),#128);
#128=MANIFOLD_SOLID_BREP('Blade_04',#3764);
#184=FACE_BOUND('',#807,.T.);
#185=FACE_BOUND('',#808,.T.);
#327=PLANE('',#4334);
#328=PLANE('',#4335);
#329=PLANE('',#4336);
#330=PLANE('',#4343);
#331=PLANE('',#4346);
#332=PLANE('',#4351);
#536=FACE_OUTER_BOUND('',#804,.T.);
#537=FACE_OUTER_BOUND('',#805,.T.);
#538=FACE_OUTER_BOUND('',#806,.T.);
#539=FACE_OUTER_BOUND('',#809,.T.);
#540=FACE_OUTER_BOUND('',#810,.T.);
#541=FACE_OUTER_BOUND('',#811,.T.);
#542=FACE_OUTER_BOUND('',#812,.T.);
#543=FACE_OUTER_BOUND('',#813,.T.);
#544=FACE_OUTER_BOUND('',#814,.T.);
#545=FACE_OUTER_BOUND('',#815,.T.);
#804=EDGE_LOOP('',(#3442,#3443,#3444,#3445));
#805=EDGE_LOOP('',(#3446,#3447,#3448,#3449));
#806=EDGE_LOOP('',(#3450,#3451,#3452,#3453));
#807=EDGE_LOOP('',(#3454));
#808=EDGE_LOOP('',(#3455));
#809=EDGE_LOOP('',(#3456,#3457,#3458,#3459));
#810=EDGE_LOOP('',(#3460));
#811=EDGE_LOOP('',(#3461,#3462,#3463,#3464));
#812=EDGE_LOOP('',(#3465));
#813=EDGE_LOOP('',(#3466,#3467,#3468,#3469));
#814=EDGE_LOOP('',(#3470,#3471,#3472,#3473));
#815=EDGE_LOOP('',(#3474,#3475,#3476,#3477));
#1024=CIRCLE('',#4337,33.8);
#1025=CIRCLE('',#4338,4.99999999999999);
#1026=CIRCLE('',#4339,1.1);
#1027=CIRCLE('',#4340,1.1);
#1028=CIRCLE('',#4342,1.1);
#1029=CIRCLE('',#4345,1.1);
#1030=CIRCLE('',#4348,4.99999999999999);
#1031=CIRCLE('',#4350,33.8);
#1308=LINE('',#6674,#1594);
#1309=LINE('',#6676,#1595);
#1310=LINE('',#6678,#1596);
#1311=LINE('',#6679,#1597);
#1312=LINE('',#6683,#1598);
#1313=LINE('',#6685,#1599);
#1314=LINE('',#6687,#1600);
#1315=LINE('',#6688,#1601);
#1316=LINE('',#6699,#1602);
#1317=LINE('',#6704,#1603);
#1594=VECTOR('',#5493,10.);
#1595=VECTOR('',#5494,10.);
#1596=VECTOR('',#5495,10.);
#1597=VECTOR('',#5496,10.);
#1598=VECTOR('',#5499,10.);
#1599=VECTOR('',#5500,10.);
#1600=VECTOR('',#5501,10.);
#1601=VECTOR('',#5502,10.);
#1602=VECTOR('',#5517,1.1);
#1603=VECTOR('',#5524,1.1);
#1933=VERTEX_POINT('',#6672);
#1934=VERTEX_POINT('',#6673);
#1935=VERTEX_POINT('',#6675);
#1936=VERTEX_POINT('',#6677);
#1937=VERTEX_POINT('',#6681);
#1938=VERTEX_POINT('',#6682);
#1939=VERTEX_POINT('',#6684);
#1940=VERTEX_POINT('',#6686);
#1941=VERTEX_POINT('',#6692);
#1942=VERTEX_POINT('',#6694);
#1943=VERTEX_POINT('',#6697);
#1944=VERTEX_POINT('',#6702);
#2438=EDGE_CURVE('',#1933,#1934,#1308,.T.);
#2439=EDGE_CURVE('',#1935,#1933,#1309,.T.);
#2440=EDGE_CURVE('',#1936,#1935,#1310,.T.);
#2441=EDGE_CURVE('',#1934,#1936,#1311,.T.);
#2442=EDGE_CURVE('',#1937,#1938,#1312,.T.);
#2443=EDGE_CURVE('',#1939,#1937,#1313,.T.);
#2444=EDGE_CURVE('',#1940,#1939,#1314,.T.);
#2445=EDGE_CURVE('',#1938,#1940,#1315,.T.);
#2446=EDGE_CURVE('',#1937,#1934,#1024,.T.);
#2447=EDGE_CURVE('',#1933,#1938,#1025,.T.);
#2448=EDGE_CURVE('',#1941,#1941,#1026,.T.);
#2449=EDGE_CURVE('',#1942,#1942,#1027,.T.);
#2450=EDGE_CURVE('',#1943,#1943,#1028,.T.);
#2451=EDGE_CURVE('',#1943,#1941,#1316,.T.);
#2452=EDGE_CURVE('',#1944,#1944,#1029,.T.);
#2453=EDGE_CURVE('',#1944,#1942,#1317,.T.);
#2454=EDGE_CURVE('',#1935,#1940,#1030,.T.);
#2455=EDGE_CURVE('',#1939,#1936,#1031,.T.);
#3442=ORIENTED_EDGE('',*,*,#2438,.F.);
#3443=ORIENTED_EDGE('',*,*,#2439,.F.);
#3444=ORIENTED_EDGE('',*,*,#2440,.F.);
#3445=ORIENTED_EDGE('',*,*,#2441,.F.);
#3446=ORIENTED_EDGE('',*,*,#2442,.F.);
#3447=ORIENTED_EDGE('',*,*,#2443,.F.);
#3448=ORIENTED_EDGE('',*,*,#2444,.F.);
#3449=ORIENTED_EDGE('',*,*,#2445,.F.);
#3450=ORIENTED_EDGE('',*,*,#2438,.T.);
#3451=ORIENTED_EDGE('',*,*,#2446,.F.);
#3452=ORIENTED_EDGE('',*,*,#2442,.T.);
#3453=ORIENTED_EDGE('',*,*,#2447,.F.);
#3454=ORIENTED_EDGE('',*,*,#2448,.T.);
#3455=ORIENTED_EDGE('',*,*,#2449,.T.);
#3456=ORIENTED_EDGE('',*,*,#2450,.F.);
#3457=ORIENTED_EDGE('',*,*,#2451,.T.);
#3458=ORIENTED_EDGE('',*,*,#2448,.F.);
#3459=ORIENTED_EDGE('',*,*,#2451,.F.);
#3460=ORIENTED_EDGE('',*,*,#2450,.T.);
#3461=ORIENTED_EDGE('',*,*,#2452,.F.);
#3462=ORIENTED_EDGE('',*,*,#2453,.T.);
#3463=ORIENTED_EDGE('',*,*,#2449,.F.);
#3464=ORIENTED_EDGE('',*,*,#2453,.F.);
#3465=ORIENTED_EDGE('',*,*,#2452,.T.);
#3466=ORIENTED_EDGE('',*,*,#2439,.T.);
#3467=ORIENTED_EDGE('',*,*,#2447,.T.);
#3468=ORIENTED_EDGE('',*,*,#2445,.T.);
#3469=ORIENTED_EDGE('',*,*,#2454,.F.);
#3470=ORIENTED_EDGE('',*,*,#2441,.T.);
#3471=ORIENTED_EDGE('',*,*,#2455,.F.);
#3472=ORIENTED_EDGE('',*,*,#2443,.T.);
#3473=ORIENTED_EDGE('',*,*,#2446,.T.);
#3474=ORIENTED_EDGE('',*,*,#2440,.T.);
#3475=ORIENTED_EDGE('',*,*,#2454,.T.);
#3476=ORIENTED_EDGE('',*,*,#2444,.T.);
#3477=ORIENTED_EDGE('',*,*,#2455,.T.);
#3535=CYLINDRICAL_SURFACE('',#4341,1.1);
#3536=CYLINDRICAL_SURFACE('',#4344,1.1);
#3537=CYLINDRICAL_SURFACE('',#4347,4.99999999999999);
#3538=CYLINDRICAL_SURFACE('',#4349,33.8);
#3742=ADVANCED_FACE('',(#536),#327,.F.);
#3743=ADVANCED_FACE('',(#537),#328,.F.);
#3744=ADVANCED_FACE('',(#538,#184,#185),#329,.F.);
#3745=ADVANCED_FACE('',(#539),#3535,.T.);
#3746=ADVANCED_FACE('',(#540),#330,.F.);
#3747=ADVANCED_FACE('',(#541),#3536,.T.);
#3748=ADVANCED_FACE('',(#542),#331,.F.);
#3749=ADVANCED_FACE('',(#543),#3537,.F.);
#3750=ADVANCED_FACE('',(#544),#3538,.T.);
#3751=ADVANCED_FACE('',(#545),#332,.T.);
#3764=CLOSED_SHELL('',(#3742,#3743,#3744,#3745,#3746,#3747,#3748,#3749,
#3750,#3751));
#4333=AXIS2_PLACEMENT_3D('',#6670,#5489,#5490);
#4334=AXIS2_PLACEMENT_3D('',#6671,#5491,#5492);
#4335=AXIS2_PLACEMENT_3D('',#6680,#5497,#5498);
#4336=AXIS2_PLACEMENT_3D('',#6689,#5503,#5504);
#4337=AXIS2_PLACEMENT_3D('',#6690,#5505,#5506);
#4338=AXIS2_PLACEMENT_3D('',#6691,#5507,#5508);
#4339=AXIS2_PLACEMENT_3D('',#6693,#5509,#5510);
#4340=AXIS2_PLACEMENT_3D('',#6695,#5511,#5512);
#4341=AXIS2_PLACEMENT_3D('',#6696,#5513,#5514);
#4342=AXIS2_PLACEMENT_3D('',#6698,#5515,#5516);
#4343=AXIS2_PLACEMENT_3D('',#6700,#5518,#5519);
#4344=AXIS2_PLACEMENT_3D('',#6701,#5520,#5521);
#4345=AXIS2_PLACEMENT_3D('',#6703,#5522,#5523);
#4346=AXIS2_PLACEMENT_3D('',#6705,#5525,#5526);
#4347=AXIS2_PLACEMENT_3D('',#6706,#5527,#5528);
#4348=AXIS2_PLACEMENT_3D('',#6707,#5529,#5530);
#4349=AXIS2_PLACEMENT_3D('',#6708,#5531,#5532);
#4350=AXIS2_PLACEMENT_3D('',#6709,#5533,#5534);
#4351=AXIS2_PLACEMENT_3D('',#6710,#5535,#5536);
#5489=DIRECTION('axis',(0.,0.,1.));
#5490=DIRECTION('refdir',(1.,0.,0.));
#5491=DIRECTION('center_axis',(-2.22044604925031E-16,0.,-1.));
#5492=DIRECTION('ref_axis',(-1.,0.,2.22044604925031E-16));
#5493=DIRECTION('',(-1.,0.,2.22044604925031E-16));
#5494=DIRECTION('',(0.,-1.,0.));
#5495=DIRECTION('',(1.,0.,-2.22044604925031E-16));
#5496=DIRECTION('',(0.,1.,0.));
#5497=DIRECTION('center_axis',(-0.707106781186547,0.,0.707106781186548));
#5498=DIRECTION('ref_axis',(0.707106781186548,0.,0.707106781186547));
#5499=DIRECTION('',(0.707106781186548,0.,0.707106781186547));
#5500=DIRECTION('',(0.,-1.,0.));
#5501=DIRECTION('',(-0.707106781186548,0.,-0.707106781186547));
#5502=DIRECTION('',(0.,1.,0.));
#5503=DIRECTION('center_axis',(0.,1.,0.));
#5504=DIRECTION('ref_axis',(-0.707106781186547,0.,0.707106781186548));
#5505=DIRECTION('center_axis',(0.,1.,0.));
#5506=DIRECTION('ref_axis',(-0.707106781186547,0.,0.707106781186548));
#5507=DIRECTION('center_axis',(0.,-1.,0.));
#5508=DIRECTION('ref_axis',(-0.707106781186547,0.,0.707106781186548));
#5509=DIRECTION('center_axis',(0.,1.,0.));
#5510=DIRECTION('ref_axis',(-0.707106781186547,0.,0.707106781186547));
#5511=DIRECTION('center_axis',(0.,1.,0.));
#5512=DIRECTION('ref_axis',(-0.707106781186547,0.,0.707106781186548));
#5513=DIRECTION('center_axis',(0.,-1.,0.));
#5514=DIRECTION('ref_axis',(-0.707106781186547,0.,0.707106781186547));
#5515=DIRECTION('center_axis',(0.,-1.,0.));
#5516=DIRECTION('ref_axis',(-0.707106781186547,0.,0.707106781186547));
#5517=DIRECTION('',(0.,1.,0.));
#5518=DIRECTION('center_axis',(0.,1.,0.));
#5519=DIRECTION('ref_axis',(-0.707106781186547,0.,0.707106781186548));
#5520=DIRECTION('center_axis',(0.,-1.,0.));
#5521=DIRECTION('ref_axis',(-0.707106781186547,0.,0.707106781186548));
#5522=DIRECTION('center_axis',(0.,-1.,0.));
#5523=DIRECTION('ref_axis',(-0.707106781186547,0.,0.707106781186548));
#5524=DIRECTION('',(0.,1.,0.));
#5525=DIRECTION('center_axis',(0.,1.,0.));
#5526=DIRECTION('ref_axis',(-0.707106781186547,0.,0.707106781186548));
#5527=DIRECTION('center_axis',(0.,1.,0.));
#5528=DIRECTION('ref_axis',(-0.707106781186547,0.,0.707106781186548));
#5529=DIRECTION('center_axis',(0.,-1.,0.));
#5530=DIRECTION('ref_axis',(-0.707106781186547,0.,0.707106781186548));
#5531=DIRECTION('center_axis',(0.,1.,0.));
#5532=DIRECTION('ref_axis',(-0.707106781186547,0.,0.707106781186548));
#5533=DIRECTION('center_axis',(0.,1.,0.));
#5534=DIRECTION('ref_axis',(-0.707106781186547,0.,0.707106781186548));
#5535=DIRECTION('center_axis',(0.,1.,0.));
#5536=DIRECTION('ref_axis',(-0.707106781186547,0.,0.707106781186548));
#6670=CARTESIAN_POINT('',(0.,0.,0.));
#6671=CARTESIAN_POINT('Origin',(-5.,-3.,114.33240815703));
#6672=CARTESIAN_POINT('',(-5.,-3.,114.33240815703));
#6673=CARTESIAN_POINT('',(-33.8,-3.,114.33240815703));
#6674=CARTESIAN_POINT('',(-2.5,-3.,114.33240815703));
#6675=CARTESIAN_POINT('',(-5.,-2.9,114.33240815703));
#6676=CARTESIAN_POINT('',(-5.,-3.,114.33240815703));
#6677=CARTESIAN_POINT('',(-33.8,-2.9,114.33240815703));
#6678=CARTESIAN_POINT('',(-2.5,-2.9,114.33240815703));
#6679=CARTESIAN_POINT('',(-33.8,-3.,114.33240815703));
#6680=CARTESIAN_POINT('Origin',(-23.9002092041053,-3.,90.4321989529251));
#6681=CARTESIAN_POINT('',(-23.9002092041053,-3.,90.4321989529251));
#6682=CARTESIAN_POINT('',(-3.53553390593273,-3.,110.796874251098));
#6683=CARTESIAN_POINT('',(-11.9501046020527,-3.,102.382303554978));
#6684=CARTESIAN_POINT('',(-23.9002092041053,-2.9,90.4321989529251));
#6685=CARTESIAN_POINT('',(-23.9002092041053,-3.,90.4321989529251));
#6686=CARTESIAN_POINT('',(-3.53553390593273,-2.9,110.796874251098));
#6687=CARTESIAN_POINT('',(-11.9501046020527,-2.9,102.382303554978));
#6688=CARTESIAN_POINT('',(-3.53553390593273,-3.,110.796874251098));
#6689=CARTESIAN_POINT('Origin',(0.,-3.,114.33240815703));
#6690=CARTESIAN_POINT('Origin',(0.,-3.,114.33240815703));
#6691=CARTESIAN_POINT('Origin',(0.,-3.,114.33240815703));
#6692=CARTESIAN_POINT('',(-23.8644576694173,-3.,97.8281079805699));
#6693=CARTESIAN_POINT('Origin',(-24.6422751287225,-3.,98.6059254398751));
#6694=CARTESIAN_POINT('',(-28.0069405518647,-3.,108.455405624497));
#6695=CARTESIAN_POINT('Origin',(-28.7847580111699,-3.,109.233223083803));
#6696=CARTESIAN_POINT('Origin',(-24.6422751287225,-3.,98.6059254398751));
#6697=CARTESIAN_POINT('',(-23.8644576694173,-3.5,97.8281079805699));
#6698=CARTESIAN_POINT('Origin',(-24.6422751287225,-3.5,98.6059254398751));
#6699=CARTESIAN_POINT('',(-23.8644576694173,-3.,97.8281079805699));
#6700=CARTESIAN_POINT('Origin',(-24.6422751287225,-3.5,98.6059254398751));
#6701=CARTESIAN_POINT('Origin',(-28.7847580111699,-3.,109.233223083803));
#6702=CARTESIAN_POINT('',(-28.0069405518647,-3.5,108.455405624497));
#6703=CARTESIAN_POINT('Origin',(-28.7847580111699,-3.5,109.233223083803));
#6704=CARTESIAN_POINT('',(-28.0069405518647,-3.,108.455405624497));
#6705=CARTESIAN_POINT('Origin',(-28.7847580111699,-3.5,109.233223083803));
#6706=CARTESIAN_POINT('Origin',(0.,-3.,114.33240815703));
#6707=CARTESIAN_POINT('Origin',(0.,-2.9,114.33240815703));
#6708=CARTESIAN_POINT('Origin',(0.,-3.,114.33240815703));
#6709=CARTESIAN_POINT('Origin',(0.,-2.9,114.33240815703));
#6710=CARTESIAN_POINT('Origin',(0.,-2.9,114.33240815703));
#6737=UNCERTAINTY_MEASURE_WITH_UNIT(LENGTH_MEASURE(0.01),#6754,
'DISTANCE_ACCURACY_VALUE',
'Maximum model space distance between geometric entities at asserted c
onnectivities');
#6738=UNCERTAINTY_MEASURE_WITH_UNIT(LENGTH_MEASURE(0.01),#6754,
'DISTANCE_ACCURACY_VALUE',
'Maximum model space distance between geometric entities at asserted c
onnectivities');
#6752=(
GEOMETRIC_REPRESENTATION_CONTEXT(3)
GLOBAL_UNCERTAINTY_ASSIGNED_CONTEXT((#6737))
GLOBAL_UNIT_ASSIGNED_CONTEXT((#6754,#6756,#6757))
REPRESENTATION_CONTEXT('','3D')
);
#6753=(
GEOMETRIC_REPRESENTATION_CONTEXT(3)
GLOBAL_UNCERTAINTY_ASSIGNED_CONTEXT((#6738))
GLOBAL_UNIT_ASSIGNED_CONTEXT((#6754,#6756,#6757))
REPRESENTATION_CONTEXT('','3D')
);
#6754=(
LENGTH_UNIT()
NAMED_UNIT(*)
SI_UNIT(.MILLI.,.METRE.)
);
#6756=(
NAMED_UNIT(*)
PLANE_ANGLE_UNIT()
SI_UNIT($,.RADIAN.)
);
#6757=(
NAMED_UNIT(*)
SI_UNIT($,.STERADIAN.)
SOLID_ANGLE_UNIT()
);
#6771=SHAPE_DEFINITION_REPRESENTATION(#6785,#6812);
#6785=PRODUCT_DEFINITION_SHAPE('',$,#6827);
#6812=SHAPE_REPRESENTATION('',(#4333),#6752);
#6813=PRODUCT_DEFINITION_CONTEXT('part definition',#6857,'design');
#6827=PRODUCT_DEFINITION('Blade_04','Blade_04',#6841,#6813);
#6841=PRODUCT_DEFINITION_FORMATION('',$,#6872);
#6857=APPLICATION_CONTEXT(
'Core Data for Automotive Mechanical Design Process');
#6858=PRODUCT_CONTEXT('part definition',#6857,'mechanical');
#6872=PRODUCT('Blade_04','Blade_04',$,(#6858));
#6908=COLOUR_RGB('Sky Blue',0.24,0.69,0.87);
#6909=FILL_AREA_STYLE_COLOUR('',#6908);
#6910=FILL_AREA_STYLE('',(#6909));
#6911=SURFACE_STYLE_FILL_AREA(#6910);
#6912=SURFACE_SIDE_STYLE('',(#6911));
#6913=SURFACE_STYLE_USAGE(.BOTH.,#6912);
#6914=PRESENTATION_STYLE_ASSIGNMENT((#6913));
ENDSEC;
END-ISO-10303-21;
